ISO-10303-21;
HEADER;
/* Generated by software containing ST-Developer
 * from STEP Tools, Inc. (www.steptools.com) 
 */

FILE_DESCRIPTION(
/* description */ ('STEP AP203'),
/* implementation_level */ '2;1');

FILE_NAME(
/* name */ 'F03_M6x12_Low_Head_Screw.step',
/* time_stamp */ '2026-11-15T15:04:01-08:00',
/* author */ (''),
/* organization */ (''),
/* preprocessor_version */ 'ST-DEVELOPER v20.2',
/* originating_system */ 'Autodesk Translation Framework v15.17.0.0',
/* authorisation */ '');

FILE_SCHEMA (('AUTOMOTIVE_DESIGN { 1 0 10303 214 3 1 1 }'));
ENDSEC;

DATA;
#10=MECHANICAL_DESIGN_GEOMETRIC_PRESENTATION_REPRESENTATION('',(#303),#16598);
#225=SHAPE_REPRESENTATION_RELATIONSHIP('SRR','None',#16719,#249);
#249=ADVANCED_BREP_SHAPE_REPRESENTATION('',(#273),#16595);
#273=MANIFOLD_SOLID_BREP('Body1',#9808);
#303=STYLED_ITEM('',(#16829),#273);
#424=FACE_BOUND('',#2100,.T.);
#425=FACE_BOUND('',#2102,.T.);
#882=PLANE('',#10844);
#883=PLANE('',#10845);
#884=PLANE('',#10846);
#885=PLANE('',#10847);
#886=PLANE('',#10848);
#887=PLANE('',#10849);
#888=PLANE('',#10850);
#889=PLANE('',#10851);
#890=PLANE('',#10852);
#891=PLANE('',#10853);
#1428=FACE_OUTER_BOUND('',#2097,.T.);
#1429=FACE_OUTER_BOUND('',#2098,.T.);
#1430=FACE_OUTER_BOUND('',#2099,.T.);
#1431=FACE_OUTER_BOUND('',#2101,.T.);
#1432=FACE_OUTER_BOUND('',#2103,.T.);
#1433=FACE_OUTER_BOUND('',#2104,.T.);
#1434=FACE_OUTER_BOUND('',#2105,.T.);
#1435=FACE_OUTER_BOUND('',#2106,.T.);
#1436=FACE_OUTER_BOUND('',#2107,.T.);
#1437=FACE_OUTER_BOUND('',#2108,.T.);
#1438=FACE_OUTER_BOUND('',#2109,.T.);
#1439=FACE_OUTER_BOUND('',#2110,.T.);
#2097=EDGE_LOOP('',(#9031,#9032,#9033,#9034));
#2098=EDGE_LOOP('',(#9035,#9036,#9037,#9038));
#2099=EDGE_LOOP('',(#9039));
#2100=EDGE_LOOP('',(#9040,#9041,#9042,#9043,#9044,#9045));
#2101=EDGE_LOOP('',(#9046));
#2102=EDGE_LOOP('',(#9047));
#2103=EDGE_LOOP('',(#9048));
#2104=EDGE_LOOP('',(#9049,#9050,#9051,#9052));
#2105=EDGE_LOOP('',(#9053,#9054,#9055,#9056));
#2106=EDGE_LOOP('',(#9057,#9058,#9059,#9060));
#2107=EDGE_LOOP('',(#9061,#9062,#9063,#9064));
#2108=EDGE_LOOP('',(#9065,#9066,#9067,#9068));
#2109=EDGE_LOOP('',(#9069,#9070,#9071,#9072));
#2110=EDGE_LOOP('',(#9073,#9074,#9075,#9076,#9077,#9078));
#3125=LINE('',#16356,#4173);
#3126=LINE('',#16362,#4174);
#3127=LINE('',#16367,#4175);
#3128=LINE('',#16369,#4176);
#3129=LINE('',#16371,#4177);
#3130=LINE('',#16373,#4178);
#3131=LINE('',#16375,#4179);
#3132=LINE('',#16376,#4180);
#3133=LINE('',#16381,#4181);
#3134=LINE('',#16383,#4182);
#3135=LINE('',#16384,#4183);
#3136=LINE('',#16387,#4184);
#3137=LINE('',#16388,#4185);
#3138=LINE('',#16391,#4186);
#3139=LINE('',#16392,#4187);
#3140=LINE('',#16395,#4188);
#3141=LINE('',#16396,#4189);
#3142=LINE('',#16399,#4190);
#3143=LINE('',#16400,#4191);
#3144=LINE('',#16402,#4192);
#4173=VECTOR('',#13445,2.4);
#4174=VECTOR('',#13452,5.);
#4175=VECTOR('',#13457,1000.);
#4176=VECTOR('',#13458,1000.);
#4177=VECTOR('',#13459,1000.);
#4178=VECTOR('',#13460,1000.);
#4179=VECTOR('',#13461,1000.);
#4180=VECTOR('',#13462,1000.);
#4181=VECTOR('',#13469,1000.);
#4182=VECTOR('',#13470,1000.);
#4183=VECTOR('',#13471,1000.);
#4184=VECTOR('',#13474,1000.);
#4185=VECTOR('',#13475,1000.);
#4186=VECTOR('',#13478,1000.);
#4187=VECTOR('',#13479,1000.);
#4188=VECTOR('',#13482,1000.);
#4189=VECTOR('',#13483,1000.);
#4190=VECTOR('',#13486,1000.);
#4191=VECTOR('',#13487,1000.);
#4192=VECTOR('',#13490,1000.);
#4445=CIRCLE('',#10839,2.4);
#4446=CIRCLE('',#10840,2.4);
#4447=CIRCLE('',#10842,5.);
#4448=CIRCLE('',#10843,5.);
#5265=VERTEX_POINT('',#16353);
#5266=VERTEX_POINT('',#16355);
#5267=VERTEX_POINT('',#16359);
#5268=VERTEX_POINT('',#16361);
#5269=VERTEX_POINT('',#16365);
#5270=VERTEX_POINT('',#16366);
#5271=VERTEX_POINT('',#16368);
#5272=VERTEX_POINT('',#16370);
#5273=VERTEX_POINT('',#16372);
#5274=VERTEX_POINT('',#16374);
#5275=VERTEX_POINT('',#16380);
#5276=VERTEX_POINT('',#16382);
#5277=VERTEX_POINT('',#16386);
#5278=VERTEX_POINT('',#16390);
#5279=VERTEX_POINT('',#16394);
#5280=VERTEX_POINT('',#16398);
#6528=EDGE_CURVE('',#5265,#5265,#4445,.T.);
#6529=EDGE_CURVE('',#5265,#5266,#3125,.T.);
#6530=EDGE_CURVE('',#5266,#5266,#4446,.T.);
#6531=EDGE_CURVE('',#5267,#5267,#4447,.T.);
#6532=EDGE_CURVE('',#5267,#5268,#3126,.T.);
#6533=EDGE_CURVE('',#5268,#5268,#4448,.T.);
#6534=EDGE_CURVE('',#5269,#5270,#3127,.T.);
#6535=EDGE_CURVE('',#5271,#5269,#3128,.T.);
#6536=EDGE_CURVE('',#5272,#5271,#3129,.T.);
#6537=EDGE_CURVE('',#5273,#5272,#3130,.T.);
#6538=EDGE_CURVE('',#5274,#5273,#3131,.T.);
#6539=EDGE_CURVE('',#5270,#5274,#3132,.T.);
#6540=EDGE_CURVE('',#5275,#5270,#3133,.T.);
#6541=EDGE_CURVE('',#5275,#5276,#3134,.T.);
#6542=EDGE_CURVE('',#5276,#5269,#3135,.T.);
#6543=EDGE_CURVE('',#5276,#5277,#3136,.T.);
#6544=EDGE_CURVE('',#5277,#5271,#3137,.T.);
#6545=EDGE_CURVE('',#5277,#5278,#3138,.T.);
#6546=EDGE_CURVE('',#5278,#5272,#3139,.T.);
#6547=EDGE_CURVE('',#5278,#5279,#3140,.T.);
#6548=EDGE_CURVE('',#5279,#5273,#3141,.T.);
#6549=EDGE_CURVE('',#5279,#5280,#3142,.T.);
#6550=EDGE_CURVE('',#5280,#5274,#3143,.T.);
#6551=EDGE_CURVE('',#5280,#5275,#3144,.T.);
#9031=ORIENTED_EDGE('',*,*,#6528,.T.);
#9032=ORIENTED_EDGE('',*,*,#6529,.T.);
#9033=ORIENTED_EDGE('',*,*,#6530,.F.);
#9034=ORIENTED_EDGE('',*,*,#6529,.F.);
#9035=ORIENTED_EDGE('',*,*,#6531,.T.);
#9036=ORIENTED_EDGE('',*,*,#6532,.T.);
#9037=ORIENTED_EDGE('',*,*,#6533,.F.);
#9038=ORIENTED_EDGE('',*,*,#6532,.F.);
#9039=ORIENTED_EDGE('',*,*,#6531,.F.);
#9040=ORIENTED_EDGE('',*,*,#6534,.F.);
#9041=ORIENTED_EDGE('',*,*,#6535,.F.);
#9042=ORIENTED_EDGE('',*,*,#6536,.F.);
#9043=ORIENTED_EDGE('',*,*,#6537,.F.);
#9044=ORIENTED_EDGE('',*,*,#6538,.F.);
#9045=ORIENTED_EDGE('',*,*,#6539,.F.);
#9046=ORIENTED_EDGE('',*,*,#6533,.T.);
#9047=ORIENTED_EDGE('',*,*,#6528,.F.);
#9048=ORIENTED_EDGE('',*,*,#6530,.T.);
#9049=ORIENTED_EDGE('',*,*,#6534,.T.);
#9050=ORIENTED_EDGE('',*,*,#6540,.F.);
#9051=ORIENTED_EDGE('',*,*,#6541,.T.);
#9052=ORIENTED_EDGE('',*,*,#6542,.T.);
#9053=ORIENTED_EDGE('',*,*,#6535,.T.);
#9054=ORIENTED_EDGE('',*,*,#6542,.F.);
#9055=ORIENTED_EDGE('',*,*,#6543,.T.);
#9056=ORIENTED_EDGE('',*,*,#6544,.T.);
#9057=ORIENTED_EDGE('',*,*,#6536,.T.);
#9058=ORIENTED_EDGE('',*,*,#6544,.F.);
#9059=ORIENTED_EDGE('',*,*,#6545,.T.);
#9060=ORIENTED_EDGE('',*,*,#6546,.T.);
#9061=ORIENTED_EDGE('',*,*,#6537,.T.);
#9062=ORIENTED_EDGE('',*,*,#6546,.F.);
#9063=ORIENTED_EDGE('',*,*,#6547,.T.);
#9064=ORIENTED_EDGE('',*,*,#6548,.T.);
#9065=ORIENTED_EDGE('',*,*,#6538,.T.);
#9066=ORIENTED_EDGE('',*,*,#6548,.F.);
#9067=ORIENTED_EDGE('',*,*,#6549,.T.);
#9068=ORIENTED_EDGE('',*,*,#6550,.T.);
#9069=ORIENTED_EDGE('',*,*,#6539,.T.);
#9070=ORIENTED_EDGE('',*,*,#6550,.F.);
#9071=ORIENTED_EDGE('',*,*,#6551,.T.);
#9072=ORIENTED_EDGE('',*,*,#6540,.T.);
#9073=ORIENTED_EDGE('',*,*,#6541,.F.);
#9074=ORIENTED_EDGE('',*,*,#6551,.F.);
#9075=ORIENTED_EDGE('',*,*,#6549,.F.);
#9076=ORIENTED_EDGE('',*,*,#6547,.F.);
#9077=ORIENTED_EDGE('',*,*,#6545,.F.);
#9078=ORIENTED_EDGE('',*,*,#6543,.F.);
#9231=CYLINDRICAL_SURFACE('',#10838,2.4);
#9232=CYLINDRICAL_SURFACE('',#10841,5.);
#9753=ADVANCED_FACE('',(#1428),#9231,.T.);
#9754=ADVANCED_FACE('',(#1429),#9232,.T.);
#9755=ADVANCED_FACE('',(#1430,#424),#882,.F.);
#9756=ADVANCED_FACE('',(#1431,#425),#883,.T.);
#9757=ADVANCED_FACE('',(#1432),#884,.T.);
#9758=ADVANCED_FACE('',(#1433),#885,.T.);
#9759=ADVANCED_FACE('',(#1434),#886,.T.);
#9760=ADVANCED_FACE('',(#1435),#887,.T.);
#9761=ADVANCED_FACE('',(#1436),#888,.T.);
#9762=ADVANCED_FACE('',(#1437),#889,.T.);
#9763=ADVANCED_FACE('',(#1438),#890,.T.);
#9764=ADVANCED_FACE('',(#1439),#891,.F.);
#9808=CLOSED_SHELL('',(#9753,#9754,#9755,#9756,#9757,#9758,#9759,#9760,
#9761,#9762,#9763,#9764));
#10837=AXIS2_PLACEMENT_3D('',#16351,#13439,#13440);
#10838=AXIS2_PLACEMENT_3D('',#16352,#13441,#13442);
#10839=AXIS2_PLACEMENT_3D('',#16354,#13443,#13444);
#10840=AXIS2_PLACEMENT_3D('',#16357,#13446,#13447);
#10841=AXIS2_PLACEMENT_3D('',#16358,#13448,#13449);
#10842=AXIS2_PLACEMENT_3D('',#16360,#13450,#13451);
#10843=AXIS2_PLACEMENT_3D('',#16363,#13453,#13454);
#10844=AXIS2_PLACEMENT_3D('',#16364,#13455,#13456);
#10845=AXIS2_PLACEMENT_3D('',#16377,#13463,#13464);
#10846=AXIS2_PLACEMENT_3D('',#16378,#13465,#13466);
#10847=AXIS2_PLACEMENT_3D('',#16379,#13467,#13468);
#10848=AXIS2_PLACEMENT_3D('',#16385,#13472,#13473);
#10849=AXIS2_PLACEMENT_3D('',#16389,#13476,#13477);
#10850=AXIS2_PLACEMENT_3D('',#16393,#13480,#13481);
#10851=AXIS2_PLACEMENT_3D('',#16397,#13484,#13485);
#10852=AXIS2_PLACEMENT_3D('',#16401,#13488,#13489);
#10853=AXIS2_PLACEMENT_3D('',#16403,#13491,#13492);
#13439=DIRECTION('axis',(0.,0.,1.));
#13440=DIRECTION('refdir',(1.,0.,0.));
#13441=DIRECTION('center_axis',(0.,0.,-1.));
#13442=DIRECTION('ref_axis',(-1.,0.,0.));
#13443=DIRECTION('center_axis',(0.,0.,1.));
#13444=DIRECTION('ref_axis',(1.,0.,0.));
#13445=DIRECTION('',(0.,0.,1.));
#13446=DIRECTION('center_axis',(0.,0.,1.));
#13447=DIRECTION('ref_axis',(1.,0.,0.));
#13448=DIRECTION('center_axis',(0.,0.,-1.));
#13449=DIRECTION('ref_axis',(-1.,0.,0.));
#13450=DIRECTION('center_axis',(0.,0.,1.));
#13451=DIRECTION('ref_axis',(1.,0.,0.));
#13452=DIRECTION('',(0.,0.,1.));
#13453=DIRECTION('center_axis',(0.,0.,1.));
#13454=DIRECTION('ref_axis',(1.,0.,0.));
#13455=DIRECTION('center_axis',(0.,0.,1.));
#13456=DIRECTION('ref_axis',(1.,0.,0.));
#13457=DIRECTION('',(-0.5,-0.866025403784438,0.));
#13458=DIRECTION('',(0.5,-0.866025403784438,0.));
#13459=DIRECTION('',(1.,-1.87789324842145E-16,0.));
#13460=DIRECTION('',(0.5,0.866025403784438,0.));
#13461=DIRECTION('',(-0.5,0.866025403784439,0.));
#13462=DIRECTION('',(-1.,0.,0.));
#13463=DIRECTION('center_axis',(0.,0.,1.));
#13464=DIRECTION('ref_axis',(1.,0.,0.));
#13465=DIRECTION('center_axis',(0.,0.,1.));
#13466=DIRECTION('ref_axis',(1.,0.,0.));
#13467=DIRECTION('center_axis',(-0.866025403784439,0.5,0.));
#13468=DIRECTION('ref_axis',(-0.5,-0.866025403784439,0.));
#13469=DIRECTION('',(0.,0.,-1.));
#13470=DIRECTION('',(0.5,0.866025403784439,0.));
#13471=DIRECTION('',(0.,0.,-1.));
#13472=DIRECTION('center_axis',(-0.866025403784439,-0.5,0.));
#13473=DIRECTION('ref_axis',(0.5,-0.866025403784439,0.));
#13474=DIRECTION('',(-0.5,0.866025403784439,0.));
#13475=DIRECTION('',(0.,0.,-1.));
#13476=DIRECTION('center_axis',(-1.87789324842145E-16,-1.,0.));
#13477=DIRECTION('ref_axis',(1.,-1.87789324842145E-16,0.));
#13478=DIRECTION('',(-1.,1.87789324842145E-16,0.));
#13479=DIRECTION('',(0.,0.,-1.));
#13480=DIRECTION('center_axis',(0.866025403784438,-0.5,0.));
#13481=DIRECTION('ref_axis',(0.5,0.866025403784438,0.));
#13482=DIRECTION('',(-0.5,-0.866025403784438,0.));
#13483=DIRECTION('',(0.,0.,-1.));
#13484=DIRECTION('center_axis',(0.866025403784439,0.5,0.));
#13485=DIRECTION('ref_axis',(-0.5,0.866025403784439,0.));
#13486=DIRECTION('',(0.5,-0.866025403784439,0.));
#13487=DIRECTION('',(0.,0.,-1.));
#13488=DIRECTION('center_axis',(0.,1.,0.));
#13489=DIRECTION('ref_axis',(0.,0.,1.));
#13490=DIRECTION('',(1.,0.,0.));
#13491=DIRECTION('center_axis',(0.,0.,1.));
#13492=DIRECTION('ref_axis',(1.,0.,0.));
#16351=CARTESIAN_POINT('',(0.,0.,0.));
#16352=CARTESIAN_POINT('Origin',(0.,0.,15.));
#16353=CARTESIAN_POINT('',(2.4,-2.93915231795365E-16,3.));
#16354=CARTESIAN_POINT('Origin',(0.,0.,3.));
#16355=CARTESIAN_POINT('',(2.4,-2.93915231795365E-16,15.));
#16356=CARTESIAN_POINT('',(2.4,-2.93915231795365E-16,15.));
#16357=CARTESIAN_POINT('Origin',(0.,0.,15.));
#16358=CARTESIAN_POINT('Origin',(0.,0.,3.));
#16359=CARTESIAN_POINT('',(5.,-6.12323399573677E-16,0.));
#16360=CARTESIAN_POINT('Origin',(0.,0.,0.));
#16361=CARTESIAN_POINT('',(5.,-6.12323399573677E-16,3.));
#16362=CARTESIAN_POINT('',(5.,-6.12323399573677E-16,3.));
#16363=CARTESIAN_POINT('Origin',(0.,0.,3.));
#16364=CARTESIAN_POINT('Origin',(0.,0.,0.));
#16365=CARTESIAN_POINT('',(2.3094010767585,0.,0.));
#16366=CARTESIAN_POINT('',(1.15470053837925,-2.,0.));
#16367=CARTESIAN_POINT('',(1.73205080756888,-1.,0.));
#16368=CARTESIAN_POINT('',(1.15470053837925,2.,0.));
#16369=CARTESIAN_POINT('',(1.73205080756888,1.,0.));
#16370=CARTESIAN_POINT('',(-1.15470053837925,2.,0.));
#16371=CARTESIAN_POINT('',(3.7557864968429E-16,2.,0.));
#16372=CARTESIAN_POINT('',(-2.3094010767585,2.82820063659975E-16,0.));
#16373=CARTESIAN_POINT('',(-1.73205080756888,1.,0.));
#16374=CARTESIAN_POINT('',(-1.15470053837925,-2.,0.));
#16375=CARTESIAN_POINT('',(-1.73205080756888,-1.,0.));
#16376=CARTESIAN_POINT('',(0.,-2.,0.));
#16377=CARTESIAN_POINT('Origin',(0.,0.,3.));
#16378=CARTESIAN_POINT('Origin',(0.,0.,15.));
#16379=CARTESIAN_POINT('Origin',(1.15470053837925,-2.,2.));
#16380=CARTESIAN_POINT('',(1.15470053837925,-2.,2.));
#16381=CARTESIAN_POINT('',(1.15470053837925,-2.,2.));
#16382=CARTESIAN_POINT('',(2.3094010767585,0.,2.));
#16383=CARTESIAN_POINT('',(1.15470053837925,-2.,2.));
#16384=CARTESIAN_POINT('',(2.3094010767585,0.,2.));
#16385=CARTESIAN_POINT('Origin',(2.3094010767585,0.,2.));
#16386=CARTESIAN_POINT('',(1.15470053837925,2.,2.));
#16387=CARTESIAN_POINT('',(2.3094010767585,0.,2.));
#16388=CARTESIAN_POINT('',(1.15470053837925,2.,2.));
#16389=CARTESIAN_POINT('Origin',(1.15470053837925,2.,2.));
#16390=CARTESIAN_POINT('',(-1.15470053837925,2.,2.));
#16391=CARTESIAN_POINT('',(1.15470053837925,2.,2.));
#16392=CARTESIAN_POINT('',(-1.15470053837925,2.,2.));
#16393=CARTESIAN_POINT('Origin',(-1.15470053837925,2.,2.));
#16394=CARTESIAN_POINT('',(-2.3094010767585,2.82820063659975E-16,2.));
#16395=CARTESIAN_POINT('',(-1.15470053837925,2.,2.));
#16396=CARTESIAN_POINT('',(-2.3094010767585,2.82820063659975E-16,2.));
#16397=CARTESIAN_POINT('Origin',(-2.3094010767585,2.82820063659975E-16,
2.));
#16398=CARTESIAN_POINT('',(-1.15470053837925,-2.,2.));
#16399=CARTESIAN_POINT('',(-2.3094010767585,2.82820063659975E-16,2.));
#16400=CARTESIAN_POINT('',(-1.15470053837925,-2.,2.));
#16401=CARTESIAN_POINT('Origin',(-1.15470053837925,-2.,2.));
#16402=CARTESIAN_POINT('',(-1.15470053837925,-2.,2.));
#16403=CARTESIAN_POINT('Origin',(0.,0.,2.));
#16569=UNCERTAINTY_MEASURE_WITH_UNIT(LENGTH_MEASURE(0.01),#16599,
'DISTANCE_ACCURACY_VALUE',
'Maximum model space distance between geometric entities at asserted c
onnectivities');
#16572=UNCERTAINTY_MEASURE_WITH_UNIT(LENGTH_MEASURE(0.01),#16599,
'DISTANCE_ACCURACY_VALUE',
'Maximum model space distance between geometric entities at asserted c
onnectivities');
#16595=(
GEOMETRIC_REPRESENTATION_CONTEXT(3)
GLOBAL_UNCERTAINTY_ASSIGNED_CONTEXT((#16569))
GLOBAL_UNIT_ASSIGNED_CONTEXT((#16599,#16601,#16602))
REPRESENTATION_CONTEXT('','3D')
);
#16598=(
GEOMETRIC_REPRESENTATION_CONTEXT(3)
GLOBAL_UNCERTAINTY_ASSIGNED_CONTEXT((#16572))
GLOBAL_UNIT_ASSIGNED_CONTEXT((#16599,#16601,#16602))
REPRESENTATION_CONTEXT('','3D')
);
#16599=(
LENGTH_UNIT()
NAMED_UNIT(*)
SI_UNIT(.MILLI.,.METRE.)
);
#16601=(
NAMED_UNIT(*)
PLANE_ANGLE_UNIT()
SI_UNIT($,.RADIAN.)
);
#16602=(
NAMED_UNIT(*)
SI_UNIT($,.STERADIAN.)
SOLID_ANGLE_UNIT()
);
#16625=SHAPE_DEFINITION_REPRESENTATION(#16650,#16719);
#16650=PRODUCT_DEFINITION_SHAPE('',$,#16745);
#16719=SHAPE_REPRESENTATION('',(#10837),#16595);
#16722=PRODUCT_DEFINITION_CONTEXT('part definition',#16799,'design');
#16745=PRODUCT_DEFINITION('F03_M6x12_Low_Head_Screw',
'F03_M6x12_Low_Head_Screw',#16770,#16722);
#16770=PRODUCT_DEFINITION_FORMATION('',$,#16823);
#16799=APPLICATION_CONTEXT(
'Core Data for Automotive Mechanical Design Process');
#16800=PRODUCT_CONTEXT('part definition',#16799,'mechanical');
#16823=PRODUCT('F03_M6x12_Low_Head_Screw','F03_M6x12_Low_Head_Screw',$,
(#16800));
#16829=PRESENTATION_STYLE_ASSIGNMENT((#16838));
#16838=SURFACE_STYLE_USAGE(.BOTH.,#16847);
#16847=SURFACE_SIDE_STYLE('',(#16856));
#16856=SURFACE_STYLE_FILL_AREA(#16865);
#16865=FILL_AREA_STYLE('Light Gray',(#16874));
#16874=FILL_AREA_STYLE_COLOUR('Light Gray',#16883);
#16883=COLOUR_RGB('Light Gray',0.827450980392157,0.827450980392157,0.827450980392157);
ENDSEC;
END-ISO-10303-21;
